ISO-10303-21;
HEADER;
/* Generated by software containing ST-Developer
 * from STEP Tools, Inc. (www.steptools.com) 
 */

FILE_DESCRIPTION(
/* description */ ('Belt tensioner idler arm'),
/* implementation_level */ '2;1');

FILE_NAME(
/* name */ 'Hex Nut - M5.step',
/* time_stamp */ '2026-10-28T03:22:15-07:00',
/* author */ (''),
/* organization */ (''),
/* preprocessor_version */ 'ST-DEVELOPER v20.2',
/* originating_system */ 'Autodesk Translation Framework v15.17.0.0',
/* authorisation */ '');

FILE_SCHEMA (('AUTOMOTIVE_DESIGN { 1 0 10303 214 3 1 1 }'));
ENDSEC;

DATA;
#10=MECHANICAL_DESIGN_GEOMETRIC_PRESENTATION_REPRESENTATION('',(#457),#12779);
#273=(
BOUNDED_CURVE()
B_SPLINE_CURVE(2,(#10544,#10545,#10546),.UNSPECIFIED.,.F.,.F.)
B_SPLINE_CURVE_WITH_KNOTS((3,3),(0.140651836354967,0.670383167684795),
 .UNSPECIFIED.)
CURVE()
GEOMETRIC_REPRESENTATION_ITEM()
RATIONAL_B_SPLINE_CURVE((1.11602540378444,1.28867513459481,1.11602540378444))
REPRESENTATION_ITEM('')
);
#274=(
BOUNDED_CURVE()
B_SPLINE_CURVE(2,(#10548,#10549,#10550),.UNSPECIFIED.,.F.,.F.)
B_SPLINE_CURVE_WITH_KNOTS((3,3),(0.140651836354967,0.670383167684795),
 .UNSPECIFIED.)
CURVE()
GEOMETRIC_REPRESENTATION_ITEM()
RATIONAL_B_SPLINE_CURVE((1.11602540378444,1.28867513459481,1.11602540378444))
REPRESENTATION_ITEM('')
);
#275=(
BOUNDED_CURVE()
B_SPLINE_CURVE(2,(#10555,#10556,#10557),.UNSPECIFIED.,.F.,.F.)
B_SPLINE_CURVE_WITH_KNOTS((3,3),(0.140651836354967,0.670383167684795),
 .UNSPECIFIED.)
CURVE()
GEOMETRIC_REPRESENTATION_ITEM()
RATIONAL_B_SPLINE_CURVE((1.11602540378444,1.28867513459481,1.11602540378444))
REPRESENTATION_ITEM('')
);
#276=(
BOUNDED_CURVE()
B_SPLINE_CURVE(2,(#10559,#10560,#10561),.UNSPECIFIED.,.F.,.F.)
B_SPLINE_CURVE_WITH_KNOTS((3,3),(0.140651836354967,0.670383167684795),
 .UNSPECIFIED.)
CURVE()
GEOMETRIC_REPRESENTATION_ITEM()
RATIONAL_B_SPLINE_CURVE((1.11602540378444,1.28867513459481,1.11602540378444))
REPRESENTATION_ITEM('')
);
#277=(
BOUNDED_CURVE()
B_SPLINE_CURVE(2,(#10563,#10564,#10565),.UNSPECIFIED.,.F.,.F.)
B_SPLINE_CURVE_WITH_KNOTS((3,3),(0.140651836354967,0.670383167684795),
 .UNSPECIFIED.)
CURVE()
GEOMETRIC_REPRESENTATION_ITEM()
RATIONAL_B_SPLINE_CURVE((1.11602540378444,1.28867513459481,1.11602540378444))
REPRESENTATION_ITEM('')
);
#278=(
BOUNDED_CURVE()
B_SPLINE_CURVE(2,(#10566,#10567,#10568),.UNSPECIFIED.,.F.,.F.)
B_SPLINE_CURVE_WITH_KNOTS((3,3),(0.140651836354967,0.670383167684795),
 .UNSPECIFIED.)
CURVE()
GEOMETRIC_REPRESENTATION_ITEM()
RATIONAL_B_SPLINE_CURVE((1.11602540378444,1.28867513459481,1.11602540378444))
REPRESENTATION_ITEM('')
);
#279=(
BOUNDED_CURVE()
B_SPLINE_CURVE(2,(#10575,#10576,#10577),.UNSPECIFIED.,.F.,.F.)
B_SPLINE_CURVE_WITH_KNOTS((3,3),(0.140651836354967,0.670383167684795),
 .UNSPECIFIED.)
CURVE()
GEOMETRIC_REPRESENTATION_ITEM()
RATIONAL_B_SPLINE_CURVE((1.11602540378444,1.28867513459481,1.11602540378444))
REPRESENTATION_ITEM('')
);
#280=(
BOUNDED_CURVE()
B_SPLINE_CURVE(2,(#10579,#10580,#10581),.UNSPECIFIED.,.F.,.F.)
B_SPLINE_CURVE_WITH_KNOTS((3,3),(0.140651836354967,0.670383167684796),
 .UNSPECIFIED.)
CURVE()
GEOMETRIC_REPRESENTATION_ITEM()
RATIONAL_B_SPLINE_CURVE((1.11602540378444,1.28867513459481,1.11602540378444))
REPRESENTATION_ITEM('')
);
#281=(
BOUNDED_CURVE()
B_SPLINE_CURVE(2,(#10583,#10584,#10585),.UNSPECIFIED.,.F.,.F.)
B_SPLINE_CURVE_WITH_KNOTS((3,3),(0.140651836354967,0.670383167684795),
 .UNSPECIFIED.)
CURVE()
GEOMETRIC_REPRESENTATION_ITEM()
RATIONAL_B_SPLINE_CURVE((1.11602540378444,1.28867513459481,1.11602540378444))
REPRESENTATION_ITEM('')
);
#282=(
BOUNDED_CURVE()
B_SPLINE_CURVE(2,(#10587,#10588,#10589),.UNSPECIFIED.,.F.,.F.)
B_SPLINE_CURVE_WITH_KNOTS((3,3),(0.140651836354967,0.670383167684795),
 .UNSPECIFIED.)
CURVE()
GEOMETRIC_REPRESENTATION_ITEM()
RATIONAL_B_SPLINE_CURVE((1.11602540378444,1.28867513459482,1.11602540378444))
REPRESENTATION_ITEM('')
);
#283=(
BOUNDED_CURVE()
B_SPLINE_CURVE(2,(#10591,#10592,#10593),.UNSPECIFIED.,.F.,.F.)
B_SPLINE_CURVE_WITH_KNOTS((3,3),(0.140651836354967,0.670383167684795),
 .UNSPECIFIED.)
CURVE()
GEOMETRIC_REPRESENTATION_ITEM()
RATIONAL_B_SPLINE_CURVE((1.11602540378444,1.28867513459481,1.11602540378444))
REPRESENTATION_ITEM('')
);
#284=(
BOUNDED_CURVE()
B_SPLINE_CURVE(2,(#10594,#10595,#10596),.UNSPECIFIED.,.F.,.F.)
B_SPLINE_CURVE_WITH_KNOTS((3,3),(0.140651836354967,0.670383167684795),
 .UNSPECIFIED.)
CURVE()
GEOMETRIC_REPRESENTATION_ITEM()
RATIONAL_B_SPLINE_CURVE((1.11602540378444,1.28867513459481,1.11602540378444))
REPRESENTATION_ITEM('')
);
#298=CONICAL_SURFACE('',#6767,0.47094010767585,1.0471975511966);
#299=CONICAL_SURFACE('',#6769,0.47094010767585,1.0471975511966);
#389=SHAPE_REPRESENTATION_RELATIONSHIP('SRR','None',#12935,#423);
#423=ADVANCED_BREP_SHAPE_REPRESENTATION('',(#498),#12752);
#457=STYLED_ITEM('',(#13191),#498);
#498=MANIFOLD_SOLID_BREP('Body1',#6192);
#559=FACE_BOUND('',#1337,.T.);
#560=FACE_BOUND('',#1339,.T.);
#721=PLANE('',#6771);
#722=PLANE('',#6772);
#723=PLANE('',#6773);
#724=PLANE('',#6777);
#725=PLANE('',#6778);
#726=PLANE('',#6779);
#727=PLANE('',#6780);
#728=PLANE('',#6781);
#928=FACE_OUTER_BOUND('',#1327,.T.);
#929=FACE_OUTER_BOUND('',#1328,.T.);
#930=FACE_OUTER_BOUND('',#1329,.T.);
#931=FACE_OUTER_BOUND('',#1330,.T.);
#932=FACE_OUTER_BOUND('',#1331,.T.);
#933=FACE_OUTER_BOUND('',#1332,.T.);
#934=FACE_OUTER_BOUND('',#1333,.T.);
#935=FACE_OUTER_BOUND('',#1334,.T.);
#936=FACE_OUTER_BOUND('',#1335,.T.);
#937=FACE_OUTER_BOUND('',#1336,.T.);
#938=FACE_OUTER_BOUND('',#1338,.T.);
#1327=EDGE_LOOP('',(#4440,#4441,#4442,#4443,#4444,#4445,#4446,#4447,#4448));
#1328=EDGE_LOOP('',(#4449,#4450,#4451,#4452,#4453,#4454,#4455,#4456,#4457));
#1329=EDGE_LOOP('',(#4458,#4459,#4460,#4461));
#1330=EDGE_LOOP('',(#4462,#4463,#4464,#4465));
#1331=EDGE_LOOP('',(#4466,#4467,#4468,#4469));
#1332=EDGE_LOOP('',(#4470,#4471,#4472,#4473));
#1333=EDGE_LOOP('',(#4474,#4475,#4476,#4477));
#1334=EDGE_LOOP('',(#4478,#4479,#4480,#4481));
#1335=EDGE_LOOP('',(#4482,#4483,#4484,#4485));
#1336=EDGE_LOOP('',(#4486));
#1337=EDGE_LOOP('',(#4487));
#1338=EDGE_LOOP('',(#4488));
#1339=EDGE_LOOP('',(#4489));
#1810=LINE('',#10552,#2159);
#1811=LINE('',#10573,#2160);
#1812=LINE('',#10598,#2161);
#1813=LINE('',#10599,#2162);
#1814=LINE('',#10601,#2163);
#1815=LINE('',#10603,#2164);
#1816=LINE('',#10608,#2165);
#1817=LINE('',#10611,#2166);
#1818=LINE('',#10613,#2167);
#2159=VECTOR('',#7868,0.47094010767585);
#2160=VECTOR('',#7875,0.47094010767585);
#2161=VECTOR('',#7878,1.);
#2162=VECTOR('',#7879,1.);
#2163=VECTOR('',#7882,1.);
#2164=VECTOR('',#7885,1.);
#2165=VECTOR('',#7890,0.25);
#2166=VECTOR('',#7895,1.);
#2167=VECTOR('',#7898,1.);
#2466=CIRCLE('',#6768,0.38);
#2467=CIRCLE('',#6770,0.38);
#2468=CIRCLE('',#6775,0.2117);
#2469=CIRCLE('',#6776,0.2117);
#2883=VERTEX_POINT('',#10542);
#2884=VERTEX_POINT('',#10543);
#2885=VERTEX_POINT('',#10547);
#2886=VERTEX_POINT('',#10551);
#2887=VERTEX_POINT('',#10554);
#2888=VERTEX_POINT('',#10558);
#2889=VERTEX_POINT('',#10562);
#2890=VERTEX_POINT('',#10570);
#2891=VERTEX_POINT('',#10572);
#2892=VERTEX_POINT('',#10574);
#2893=VERTEX_POINT('',#10578);
#2894=VERTEX_POINT('',#10582);
#2895=VERTEX_POINT('',#10586);
#2896=VERTEX_POINT('',#10590);
#2897=VERTEX_POINT('',#10605);
#2898=VERTEX_POINT('',#10607);
#3475=EDGE_CURVE('',#2883,#2884,#273,.T.);
#3476=EDGE_CURVE('',#2885,#2883,#274,.T.);
#3477=EDGE_CURVE('',#2885,#2886,#1810,.T.);
#3478=EDGE_CURVE('',#2886,#2886,#2466,.T.);
#3479=EDGE_CURVE('',#2887,#2885,#275,.T.);
#3480=EDGE_CURVE('',#2888,#2887,#276,.T.);
#3481=EDGE_CURVE('',#2889,#2888,#277,.T.);
#3482=EDGE_CURVE('',#2884,#2889,#278,.T.);
#3483=EDGE_CURVE('',#2890,#2890,#2467,.T.);
#3484=EDGE_CURVE('',#2890,#2891,#1811,.T.);
#3485=EDGE_CURVE('',#2892,#2891,#279,.T.);
#3486=EDGE_CURVE('',#2893,#2892,#280,.T.);
#3487=EDGE_CURVE('',#2894,#2893,#281,.T.);
#3488=EDGE_CURVE('',#2895,#2894,#282,.T.);
#3489=EDGE_CURVE('',#2896,#2895,#283,.T.);
#3490=EDGE_CURVE('',#2891,#2896,#284,.T.);
#3491=EDGE_CURVE('',#2887,#2896,#1812,.T.);
#3492=EDGE_CURVE('',#2888,#2895,#1813,.T.);
#3493=EDGE_CURVE('',#2885,#2891,#1814,.T.);
#3494=EDGE_CURVE('',#2883,#2892,#1815,.T.);
#3495=EDGE_CURVE('',#2897,#2897,#2468,.F.);
#3496=EDGE_CURVE('',#2897,#2898,#1816,.T.);
#3497=EDGE_CURVE('',#2898,#2898,#2469,.F.);
#3498=EDGE_CURVE('',#2884,#2893,#1817,.T.);
#3499=EDGE_CURVE('',#2889,#2894,#1818,.T.);
#4440=ORIENTED_EDGE('',*,*,#3475,.F.);
#4441=ORIENTED_EDGE('',*,*,#3476,.F.);
#4442=ORIENTED_EDGE('',*,*,#3477,.T.);
#4443=ORIENTED_EDGE('',*,*,#3478,.F.);
#4444=ORIENTED_EDGE('',*,*,#3477,.F.);
#4445=ORIENTED_EDGE('',*,*,#3479,.F.);
#4446=ORIENTED_EDGE('',*,*,#3480,.F.);
#4447=ORIENTED_EDGE('',*,*,#3481,.F.);
#4448=ORIENTED_EDGE('',*,*,#3482,.F.);
#4449=ORIENTED_EDGE('',*,*,#3483,.F.);
#4450=ORIENTED_EDGE('',*,*,#3484,.T.);
#4451=ORIENTED_EDGE('',*,*,#3485,.F.);
#4452=ORIENTED_EDGE('',*,*,#3486,.F.);
#4453=ORIENTED_EDGE('',*,*,#3487,.F.);
#4454=ORIENTED_EDGE('',*,*,#3488,.F.);
#4455=ORIENTED_EDGE('',*,*,#3489,.F.);
#4456=ORIENTED_EDGE('',*,*,#3490,.F.);
#4457=ORIENTED_EDGE('',*,*,#3484,.F.);
#4458=ORIENTED_EDGE('',*,*,#3480,.T.);
#4459=ORIENTED_EDGE('',*,*,#3491,.T.);
#4460=ORIENTED_EDGE('',*,*,#3489,.T.);
#4461=ORIENTED_EDGE('',*,*,#3492,.F.);
#4462=ORIENTED_EDGE('',*,*,#3479,.T.);
#4463=ORIENTED_EDGE('',*,*,#3493,.T.);
#4464=ORIENTED_EDGE('',*,*,#3490,.T.);
#4465=ORIENTED_EDGE('',*,*,#3491,.F.);
#4466=ORIENTED_EDGE('',*,*,#3476,.T.);
#4467=ORIENTED_EDGE('',*,*,#3494,.T.);
#4468=ORIENTED_EDGE('',*,*,#3485,.T.);
#4469=ORIENTED_EDGE('',*,*,#3493,.F.);
#4470=ORIENTED_EDGE('',*,*,#3495,.F.);
#4471=ORIENTED_EDGE('',*,*,#3496,.T.);
#4472=ORIENTED_EDGE('',*,*,#3497,.T.);
#4473=ORIENTED_EDGE('',*,*,#3496,.F.);
#4474=ORIENTED_EDGE('',*,*,#3475,.T.);
#4475=ORIENTED_EDGE('',*,*,#3498,.T.);
#4476=ORIENTED_EDGE('',*,*,#3486,.T.);
#4477=ORIENTED_EDGE('',*,*,#3494,.F.);
#4478=ORIENTED_EDGE('',*,*,#3481,.T.);
#4479=ORIENTED_EDGE('',*,*,#3492,.T.);
#4480=ORIENTED_EDGE('',*,*,#3488,.T.);
#4481=ORIENTED_EDGE('',*,*,#3499,.F.);
#4482=ORIENTED_EDGE('',*,*,#3482,.T.);
#4483=ORIENTED_EDGE('',*,*,#3499,.T.);
#4484=ORIENTED_EDGE('',*,*,#3487,.T.);
#4485=ORIENTED_EDGE('',*,*,#3498,.F.);
#4486=ORIENTED_EDGE('',*,*,#3483,.T.);
#4487=ORIENTED_EDGE('',*,*,#3495,.T.);
#4488=ORIENTED_EDGE('',*,*,#3478,.T.);
#4489=ORIENTED_EDGE('',*,*,#3497,.F.);
#5689=CYLINDRICAL_SURFACE('',#6774,0.2117);
#5905=ADVANCED_FACE('',(#928),#298,.T.);
#5906=ADVANCED_FACE('',(#929),#299,.T.);
#5907=ADVANCED_FACE('',(#930),#721,.T.);
#5908=ADVANCED_FACE('',(#931),#722,.T.);
#5909=ADVANCED_FACE('',(#932),#723,.T.);
#5910=ADVANCED_FACE('',(#933),#5689,.F.);
#5911=ADVANCED_FACE('',(#934),#724,.T.);
#5912=ADVANCED_FACE('',(#935),#725,.T.);
#5913=ADVANCED_FACE('',(#936),#726,.T.);
#5914=ADVANCED_FACE('',(#937,#559),#727,.T.);
#5915=ADVANCED_FACE('',(#938,#560),#728,.F.);
#6192=CLOSED_SHELL('',(#5905,#5906,#5907,#5908,#5909,#5910,#5911,#5912,
#5913,#5914,#5915));
#6766=AXIS2_PLACEMENT_3D('',#10540,#7864,#7865);
#6767=AXIS2_PLACEMENT_3D('',#10541,#7866,#7867);
#6768=AXIS2_PLACEMENT_3D('',#10553,#7869,#7870);
#6769=AXIS2_PLACEMENT_3D('',#10569,#7871,#7872);
#6770=AXIS2_PLACEMENT_3D('',#10571,#7873,#7874);
#6771=AXIS2_PLACEMENT_3D('',#10597,#7876,#7877);
#6772=AXIS2_PLACEMENT_3D('',#10600,#7880,#7881);
#6773=AXIS2_PLACEMENT_3D('',#10602,#7883,#7884);
#6774=AXIS2_PLACEMENT_3D('',#10604,#7886,#7887);
#6775=AXIS2_PLACEMENT_3D('',#10606,#7888,#7889);
#6776=AXIS2_PLACEMENT_3D('',#10609,#7891,#7892);
#6777=AXIS2_PLACEMENT_3D('',#10610,#7893,#7894);
#6778=AXIS2_PLACEMENT_3D('',#10612,#7896,#7897);
#6779=AXIS2_PLACEMENT_3D('',#10614,#7899,#7900);
#6780=AXIS2_PLACEMENT_3D('',#10615,#7901,#7902);
#6781=AXIS2_PLACEMENT_3D('',#10616,#7903,#7904);
#7864=DIRECTION('axis',(0.,0.,1.));
#7865=DIRECTION('refdir',(1.,0.,0.));
#7866=DIRECTION('center_axis',(0.,1.,0.));
#7867=DIRECTION('ref_axis',(1.,0.,0.));
#7868=DIRECTION('',(0.866025403784439,-0.5,1.06057523872491E-16));
#7869=DIRECTION('center_axis',(0.,-1.,0.));
#7870=DIRECTION('ref_axis',(1.,0.,0.));
#7871=DIRECTION('center_axis',(0.,-1.,0.));
#7872=DIRECTION('ref_axis',(1.,0.,0.));
#7873=DIRECTION('center_axis',(0.,1.,0.));
#7874=DIRECTION('ref_axis',(1.,0.,0.));
#7875=DIRECTION('',(-0.866025403784439,-0.5,-1.06057523872491E-16));
#7876=DIRECTION('center_axis',(1.20185167898973E-16,0.,-1.));
#7877=DIRECTION('ref_axis',(-1.,0.,-1.20185167898973E-16));
#7878=DIRECTION('',(0.,1.,0.));
#7879=DIRECTION('',(0.,1.,0.));
#7880=DIRECTION('center_axis',(-0.866025403784439,0.,-0.5));
#7881=DIRECTION('ref_axis',(-0.5,0.,0.866025403784439));
#7882=DIRECTION('',(0.,1.,0.));
#7883=DIRECTION('center_axis',(-0.866025403784439,0.,0.5));
#7884=DIRECTION('ref_axis',(0.5,0.,0.866025403784439));
#7885=DIRECTION('',(0.,1.,0.));
#7886=DIRECTION('center_axis',(0.,1.,0.));
#7887=DIRECTION('ref_axis',(1.,0.,0.));
#7888=DIRECTION('center_axis',(0.,1.,0.));
#7889=DIRECTION('ref_axis',(1.,0.,0.));
#7890=DIRECTION('',(0.,-1.,0.));
#7891=DIRECTION('center_axis',(0.,1.,0.));
#7892=DIRECTION('ref_axis',(1.,0.,0.));
#7893=DIRECTION('center_axis',(-2.40370335797945E-16,0.,1.));
#7894=DIRECTION('ref_axis',(1.,0.,2.40370335797945E-16));
#7895=DIRECTION('',(0.,1.,0.));
#7896=DIRECTION('center_axis',(0.866025403784439,0.,-0.5));
#7897=DIRECTION('ref_axis',(-0.5,0.,-0.866025403784439));
#7898=DIRECTION('',(0.,1.,0.));
#7899=DIRECTION('center_axis',(0.866025403784439,0.,0.5));
#7900=DIRECTION('ref_axis',(0.5,0.,-0.866025403784439));
#7901=DIRECTION('center_axis',(0.,1.,0.));
#7902=DIRECTION('ref_axis',(1.,0.,0.));
#7903=DIRECTION('center_axis',(0.,1.,0.));
#7904=DIRECTION('ref_axis',(1.,0.,0.));
#10540=CARTESIAN_POINT('',(0.,0.,0.));
#10541=CARTESIAN_POINT('Origin',(0.,0.0525042956467857,0.));
#10542=CARTESIAN_POINT('',(-0.230940107675851,0.0472735643746089,0.4));
#10543=CARTESIAN_POINT('',(0.23094010767585,0.0472735643746089,0.4));
#10544=CARTESIAN_POINT('Ctrl Pts',(-0.230940107675851,0.0472735643746089,
0.4));
#10545=CARTESIAN_POINT('Ctrl Pts',(1.11022302462516E-16,-0.0193931022920578,
0.4));
#10546=CARTESIAN_POINT('Ctrl Pts',(0.23094010767585,0.0472735643746089,
0.4));
#10547=CARTESIAN_POINT('',(-0.461880215351701,0.0472735643746089,-5.6564012731995E-17));
#10548=CARTESIAN_POINT('Ctrl Pts',(-0.461880215351701,0.0472735643746089,
-5.6564012731995E-17));
#10549=CARTESIAN_POINT('Ctrl Pts',(-0.346410161513776,-0.0193931022920579,
0.2));
#10550=CARTESIAN_POINT('Ctrl Pts',(-0.230940107675851,0.0472735643746089,
0.4));
#10551=CARTESIAN_POINT('',(-0.38,-2.08166817117217E-17,-4.65365783675994E-17));
#10552=CARTESIAN_POINT('',(-0.47094010767585,0.0525042956467857,-5.7673529545534E-17));
#10553=CARTESIAN_POINT('Origin',(0.,0.,0.));
#10554=CARTESIAN_POINT('',(-0.23094010767585,0.0472735643746089,-0.4));
#10555=CARTESIAN_POINT('Ctrl Pts',(-0.23094010767585,0.0472735643746089,
-0.4));
#10556=CARTESIAN_POINT('Ctrl Pts',(-0.346410161513775,-0.0193931022920578,
-0.2));
#10557=CARTESIAN_POINT('Ctrl Pts',(-0.461880215351701,0.0472735643746089,
-5.6564012731995E-17));
#10558=CARTESIAN_POINT('',(0.23094010767585,0.0472735643746089,-0.4));
#10559=CARTESIAN_POINT('Ctrl Pts',(0.23094010767585,0.0472735643746089,
-0.4));
#10560=CARTESIAN_POINT('Ctrl Pts',(0.,-0.0193931022920578,-0.4));
#10561=CARTESIAN_POINT('Ctrl Pts',(-0.23094010767585,0.0472735643746089,
-0.4));
#10562=CARTESIAN_POINT('',(0.461880215351701,0.0472735643746089,0.));
#10563=CARTESIAN_POINT('Ctrl Pts',(0.461880215351701,0.0472735643746089,
0.));
#10564=CARTESIAN_POINT('Ctrl Pts',(0.346410161513776,-0.019393102292058,
-0.2));
#10565=CARTESIAN_POINT('Ctrl Pts',(0.23094010767585,0.0472735643746089,
-0.4));
#10566=CARTESIAN_POINT('Ctrl Pts',(0.23094010767585,0.0472735643746089,
0.4));
#10567=CARTESIAN_POINT('Ctrl Pts',(0.346410161513776,-0.0193931022920577,
0.2));
#10568=CARTESIAN_POINT('Ctrl Pts',(0.461880215351701,0.0472735643746089,
0.));
#10569=CARTESIAN_POINT('Origin',(0.,0.417495704353214,0.));
#10570=CARTESIAN_POINT('',(-0.38,0.47,-4.65365783675994E-17));
#10571=CARTESIAN_POINT('Origin',(0.,0.47,0.));
#10572=CARTESIAN_POINT('',(-0.461880215351701,0.422726435625391,-5.6564012731995E-17));
#10573=CARTESIAN_POINT('',(-0.47094010767585,0.417495704353214,-5.7673529545534E-17));
#10574=CARTESIAN_POINT('',(-0.230940107675851,0.422726435625391,0.4));
#10575=CARTESIAN_POINT('Ctrl Pts',(-0.230940107675851,0.422726435625391,
0.4));
#10576=CARTESIAN_POINT('Ctrl Pts',(-0.346410161513776,0.489393102292058,
0.2));
#10577=CARTESIAN_POINT('Ctrl Pts',(-0.461880215351701,0.422726435625391,
-5.6564012731995E-17));
#10578=CARTESIAN_POINT('',(0.23094010767585,0.422726435625391,0.4));
#10579=CARTESIAN_POINT('Ctrl Pts',(0.23094010767585,0.422726435625391,0.4));
#10580=CARTESIAN_POINT('Ctrl Pts',(8.32667268468867E-17,0.489393102292058,
0.4));
#10581=CARTESIAN_POINT('Ctrl Pts',(-0.230940107675851,0.422726435625391,
0.4));
#10582=CARTESIAN_POINT('',(0.461880215351701,0.422726435625391,0.));
#10583=CARTESIAN_POINT('Ctrl Pts',(0.461880215351701,0.422726435625391,
0.));
#10584=CARTESIAN_POINT('Ctrl Pts',(0.346410161513776,0.489393102292058,
0.2));
#10585=CARTESIAN_POINT('Ctrl Pts',(0.23094010767585,0.422726435625391,0.4));
#10586=CARTESIAN_POINT('',(0.23094010767585,0.422726435625391,-0.4));
#10587=CARTESIAN_POINT('Ctrl Pts',(0.23094010767585,0.422726435625391,-0.4));
#10588=CARTESIAN_POINT('Ctrl Pts',(0.346410161513775,0.489393102292058,
-0.2));
#10589=CARTESIAN_POINT('Ctrl Pts',(0.461880215351701,0.422726435625391,
0.));
#10590=CARTESIAN_POINT('',(-0.23094010767585,0.422726435625391,-0.4));
#10591=CARTESIAN_POINT('Ctrl Pts',(-0.23094010767585,0.422726435625391,
-0.4));
#10592=CARTESIAN_POINT('Ctrl Pts',(-5.55111512312578E-17,0.489393102292058,
-0.4));
#10593=CARTESIAN_POINT('Ctrl Pts',(0.23094010767585,0.422726435625391,-0.4));
#10594=CARTESIAN_POINT('Ctrl Pts',(-0.461880215351701,0.422726435625391,
-5.6564012731995E-17));
#10595=CARTESIAN_POINT('Ctrl Pts',(-0.346410161513776,0.489393102292058,
-0.2));
#10596=CARTESIAN_POINT('Ctrl Pts',(-0.23094010767585,0.422726435625391,
-0.4));
#10597=CARTESIAN_POINT('Origin',(0.23094010767585,0.,-0.4));
#10598=CARTESIAN_POINT('',(-0.23094010767585,0.,-0.4));
#10599=CARTESIAN_POINT('',(0.23094010767585,0.,-0.4));
#10600=CARTESIAN_POINT('Origin',(-0.23094010767585,0.,-0.4));
#10601=CARTESIAN_POINT('',(-0.461880215351701,0.,-5.6564012731995E-17));
#10602=CARTESIAN_POINT('Origin',(-0.461880215351701,0.,-5.6564012731995E-17));
#10603=CARTESIAN_POINT('',(-0.230940107675851,0.,0.4));
#10604=CARTESIAN_POINT('Origin',(0.,0.,0.));
#10605=CARTESIAN_POINT('',(-0.2117,0.47,2.59257727379495E-17));
#10606=CARTESIAN_POINT('Origin',(0.,0.47,0.));
#10607=CARTESIAN_POINT('',(-0.2117,0.,2.59257727379495E-17));
#10608=CARTESIAN_POINT('',(-0.2117,0.,2.59257727379495E-17));
#10609=CARTESIAN_POINT('Origin',(0.,0.,0.));
#10610=CARTESIAN_POINT('Origin',(-0.230940107675851,0.,0.4));
#10611=CARTESIAN_POINT('',(0.23094010767585,0.,0.4));
#10612=CARTESIAN_POINT('Origin',(0.461880215351701,0.,0.));
#10613=CARTESIAN_POINT('',(0.461880215351701,0.,0.));
#10614=CARTESIAN_POINT('Origin',(0.23094010767585,0.,0.4));
#10615=CARTESIAN_POINT('Origin',(0.,0.47,0.));
#10616=CARTESIAN_POINT('Origin',(0.,0.,0.));
#12712=UNCERTAINTY_MEASURE_WITH_UNIT(LENGTH_MEASURE(0.001),#12780,
'DISTANCE_ACCURACY_VALUE',
'Maximum model space distance between geometric entities at asserted c
onnectivities');
#12739=UNCERTAINTY_MEASURE_WITH_UNIT(LENGTH_MEASURE(0.001),#12780,
'DISTANCE_ACCURACY_VALUE',
'Maximum model space distance between geometric entities at asserted c
onnectivities');
#12752=(
GEOMETRIC_REPRESENTATION_CONTEXT(3)
GLOBAL_UNCERTAINTY_ASSIGNED_CONTEXT((#12712))
GLOBAL_UNIT_ASSIGNED_CONTEXT((#12780,#12782,#12783))
REPRESENTATION_CONTEXT('','3D')
);
#12779=(
GEOMETRIC_REPRESENTATION_CONTEXT(3)
GLOBAL_UNCERTAINTY_ASSIGNED_CONTEXT((#12739))
GLOBAL_UNIT_ASSIGNED_CONTEXT((#12780,#12782,#12783))
REPRESENTATION_CONTEXT('','3D')
);
#12780=(
LENGTH_UNIT()
NAMED_UNIT(*)
SI_UNIT(.CENTI.,.METRE.)
);
#12782=(
NAMED_UNIT(*)
PLANE_ANGLE_UNIT()
SI_UNIT($,.RADIAN.)
);
#12783=(
NAMED_UNIT(*)
SI_UNIT($,.STERADIAN.)
SOLID_ANGLE_UNIT()
);
#12796=SHAPE_DEFINITION_REPRESENTATION(#12835,#12935);
#12835=PRODUCT_DEFINITION_SHAPE('',$,#12975);
#12935=SHAPE_REPRESENTATION('',(#6766),#12752);
#12962=PRODUCT_DEFINITION_CONTEXT('part definition',#13081,'design');
#12975=PRODUCT_DEFINITION('Hex Nut - M5','Hex Nut - M5',#13014,#12962);
#13014=PRODUCT_DEFINITION_FORMATION('',$,#13095);
#13081=APPLICATION_CONTEXT(
'Core Data for Automotive Mechanical Design Process');
#13082=PRODUCT_CONTEXT('part definition',#13081,'mechanical');
#13095=PRODUCT('Hex Nut - M5','Hex Nut - M5','Hex Nut - M5',(#13082));
#13185=COLOUR_RGB('Black',0.12,0.14,0.17);
#13186=FILL_AREA_STYLE_COLOUR('',#13185);
#13187=FILL_AREA_STYLE('',(#13186));
#13188=SURFACE_STYLE_FILL_AREA(#13187);
#13189=SURFACE_SIDE_STYLE('',(#13188));
#13190=SURFACE_STYLE_USAGE(.BOTH.,#13189);
#13191=PRESENTATION_STYLE_ASSIGNMENT((#13190));
ENDSEC;
END-ISO-10303-21;
